ISO-10303-21;
HEADER;
/* Generated by software containing ST-Developer
 * from STEP Tools, Inc. (www.steptools.com) 
 */

FILE_DESCRIPTION(
/* description */ ('PAT-083'),
/* implementation_level */ '2;1');

FILE_NAME(
/* name */ 'Flat Washer - M8.step',
/* time_stamp */ '2026-10-29T20:18:00-07:00',
/* author */ (''),
/* organization */ (''),
/* preprocessor_version */ 'ST-DEVELOPER v20.2',
/* originating_system */ 'Autodesk Translation Framework v15.17.0.0',
/* authorisation */ '');

FILE_SCHEMA (('AUTOMOTIVE_DESIGN { 1 0 10303 214 3 1 1 }'));
ENDSEC;

DATA;
#10=MECHANICAL_DESIGN_GEOMETRIC_PRESENTATION_REPRESENTATION('',(#250),#8428);
#202=SHAPE_REPRESENTATION_RELATIONSHIP('SRR','None',#8536,#226);
#226=ADVANCED_BREP_SHAPE_REPRESENTATION('',(#272),#8425);
#250=STYLED_ITEM('',(#8712),#272);
#272=MANIFOLD_SOLID_BREP('Body1',#3698);
#351=FACE_BOUND('',#1013,.T.);
#352=FACE_BOUND('',#1015,.T.);
#476=PLANE('',#4370);
#477=PLANE('',#4371);
#701=FACE_OUTER_BOUND('',#1010,.T.);
#702=FACE_OUTER_BOUND('',#1011,.T.);
#703=FACE_OUTER_BOUND('',#1012,.T.);
#704=FACE_OUTER_BOUND('',#1014,.T.);
#1010=EDGE_LOOP('',(#3252,#3253,#3254,#3255));
#1011=EDGE_LOOP('',(#3256,#3257,#3258,#3259));
#1012=EDGE_LOOP('',(#3260));
#1013=EDGE_LOOP('',(#3261));
#1014=EDGE_LOOP('',(#3262));
#1015=EDGE_LOOP('',(#3263));
#1254=LINE('',#8205,#1498);
#1255=LINE('',#8211,#1499);
#1498=VECTOR('',#5448,0.42);
#1499=VECTOR('',#5455,0.8);
#1701=CIRCLE('',#4365,0.42);
#1702=CIRCLE('',#4366,0.42);
#1703=CIRCLE('',#4368,0.8);
#1704=CIRCLE('',#4369,0.8);
#1969=VERTEX_POINT('',#8202);
#1970=VERTEX_POINT('',#8204);
#1971=VERTEX_POINT('',#8208);
#1972=VERTEX_POINT('',#8210);
#2402=EDGE_CURVE('',#1969,#1969,#1701,.T.);
#2403=EDGE_CURVE('',#1969,#1970,#1254,.T.);
#2404=EDGE_CURVE('',#1970,#1970,#1702,.T.);
#2405=EDGE_CURVE('',#1971,#1971,#1703,.T.);
#2406=EDGE_CURVE('',#1971,#1972,#1255,.T.);
#2407=EDGE_CURVE('',#1972,#1972,#1704,.T.);
#3252=ORIENTED_EDGE('',*,*,#2402,.F.);
#3253=ORIENTED_EDGE('',*,*,#2403,.T.);
#3254=ORIENTED_EDGE('',*,*,#2404,.T.);
#3255=ORIENTED_EDGE('',*,*,#2403,.F.);
#3256=ORIENTED_EDGE('',*,*,#2405,.F.);
#3257=ORIENTED_EDGE('',*,*,#2406,.T.);
#3258=ORIENTED_EDGE('',*,*,#2407,.T.);
#3259=ORIENTED_EDGE('',*,*,#2406,.F.);
#3260=ORIENTED_EDGE('',*,*,#2405,.T.);
#3261=ORIENTED_EDGE('',*,*,#2402,.T.);
#3262=ORIENTED_EDGE('',*,*,#2407,.F.);
#3263=ORIENTED_EDGE('',*,*,#2404,.F.);
#3438=CYLINDRICAL_SURFACE('',#4364,0.42);
#3439=CYLINDRICAL_SURFACE('',#4367,0.8);
#3648=ADVANCED_FACE('',(#701),#3438,.F.);
#3649=ADVANCED_FACE('',(#702),#3439,.T.);
#3650=ADVANCED_FACE('',(#703,#351),#476,.T.);
#3651=ADVANCED_FACE('',(#704,#352),#477,.F.);
#3698=CLOSED_SHELL('',(#3648,#3649,#3650,#3651));
#4363=AXIS2_PLACEMENT_3D('',#8200,#5442,#5443);
#4364=AXIS2_PLACEMENT_3D('',#8201,#5444,#5445);
#4365=AXIS2_PLACEMENT_3D('',#8203,#5446,#5447);
#4366=AXIS2_PLACEMENT_3D('',#8206,#5449,#5450);
#4367=AXIS2_PLACEMENT_3D('',#8207,#5451,#5452);
#4368=AXIS2_PLACEMENT_3D('',#8209,#5453,#5454);
#4369=AXIS2_PLACEMENT_3D('',#8212,#5456,#5457);
#4370=AXIS2_PLACEMENT_3D('',#8213,#5458,#5459);
#4371=AXIS2_PLACEMENT_3D('',#8214,#5460,#5461);
#5442=DIRECTION('axis',(0.,0.,1.));
#5443=DIRECTION('refdir',(1.,0.,0.));
#5444=DIRECTION('center_axis',(0.,1.,0.));
#5445=DIRECTION('ref_axis',(1.,0.,0.));
#5446=DIRECTION('center_axis',(0.,-1.,0.));
#5447=DIRECTION('ref_axis',(1.,0.,0.));
#5448=DIRECTION('',(0.,-1.,0.));
#5449=DIRECTION('center_axis',(0.,-1.,0.));
#5450=DIRECTION('ref_axis',(1.,0.,0.));
#5451=DIRECTION('center_axis',(0.,1.,0.));
#5452=DIRECTION('ref_axis',(1.,0.,0.));
#5453=DIRECTION('center_axis',(0.,1.,0.));
#5454=DIRECTION('ref_axis',(1.,0.,0.));
#5455=DIRECTION('',(0.,-1.,0.));
#5456=DIRECTION('center_axis',(0.,1.,0.));
#5457=DIRECTION('ref_axis',(1.,0.,0.));
#5458=DIRECTION('center_axis',(0.,1.,0.));
#5459=DIRECTION('ref_axis',(1.,0.,0.));
#5460=DIRECTION('center_axis',(0.,1.,0.));
#5461=DIRECTION('ref_axis',(1.,0.,0.));
#8200=CARTESIAN_POINT('',(0.,0.,0.));
#8201=CARTESIAN_POINT('Origin',(0.,0.,0.));
#8202=CARTESIAN_POINT('',(-0.42,0.16,5.14351655641888E-17));
#8203=CARTESIAN_POINT('Origin',(0.,0.16,0.));
#8204=CARTESIAN_POINT('',(-0.42,0.,5.14351655641888E-17));
#8205=CARTESIAN_POINT('',(-0.42,0.,5.14351655641888E-17));
#8206=CARTESIAN_POINT('Origin',(0.,0.,0.));
#8207=CARTESIAN_POINT('Origin',(0.,0.,0.));
#8208=CARTESIAN_POINT('',(-0.8,0.16,9.79717439317883E-17));
#8209=CARTESIAN_POINT('Origin',(0.,0.16,0.));
#8210=CARTESIAN_POINT('',(-0.8,0.,9.79717439317883E-17));
#8211=CARTESIAN_POINT('',(-0.8,0.,9.79717439317883E-17));
#8212=CARTESIAN_POINT('Origin',(0.,0.,0.));
#8213=CARTESIAN_POINT('Origin',(0.,0.16,0.));
#8214=CARTESIAN_POINT('Origin',(0.,0.,0.));
#8399=UNCERTAINTY_MEASURE_WITH_UNIT(LENGTH_MEASURE(0.001),#8429,
'DISTANCE_ACCURACY_VALUE',
'Maximum model space distance between geometric entities at asserted c
onnectivities');
#8402=UNCERTAINTY_MEASURE_WITH_UNIT(LENGTH_MEASURE(0.001),#8429,
'DISTANCE_ACCURACY_VALUE',
'Maximum model space distance between geometric entities at asserted c
onnectivities');
#8425=(
GEOMETRIC_REPRESENTATION_CONTEXT(3)
GLOBAL_UNCERTAINTY_ASSIGNED_CONTEXT((#8399))
GLOBAL_UNIT_ASSIGNED_CONTEXT((#8429,#8431,#8432))
REPRESENTATION_CONTEXT('','3D')
);
#8428=(
GEOMETRIC_REPRESENTATION_CONTEXT(3)
GLOBAL_UNCERTAINTY_ASSIGNED_CONTEXT((#8402))
GLOBAL_UNIT_ASSIGNED_CONTEXT((#8429,#8431,#8432))
REPRESENTATION_CONTEXT('','3D')
);
#8429=(
LENGTH_UNIT()
NAMED_UNIT(*)
SI_UNIT(.CENTI.,.METRE.)
);
#8431=(
NAMED_UNIT(*)
PLANE_ANGLE_UNIT()
SI_UNIT($,.RADIAN.)
);
#8432=(
NAMED_UNIT(*)
SI_UNIT($,.STERADIAN.)
SOLID_ANGLE_UNIT()
);
#8455=SHAPE_DEFINITION_REPRESENTATION(#8480,#8536);
#8480=PRODUCT_DEFINITION_SHAPE('',$,#8562);
#8536=SHAPE_REPRESENTATION('',(#4363),#8425);
#8539=PRODUCT_DEFINITION_CONTEXT('part definition',#8616,'design');
#8562=PRODUCT_DEFINITION('Flat Washer - M8','Flat Washer - M8',#8587,
#8539);
#8587=PRODUCT_DEFINITION_FORMATION('',$,#8640);
#8616=APPLICATION_CONTEXT(
'Core Data for Automotive Mechanical Design Process');
#8617=PRODUCT_CONTEXT('part definition',#8616,'mechanical');
#8640=PRODUCT('Flat Washer - M8','Flat Washer - M8',
'Flat Washer - M8',(#8617));
#8706=COLOUR_RGB('Black',0.12,0.14,0.17);
#8707=FILL_AREA_STYLE_COLOUR('',#8706);
#8708=FILL_AREA_STYLE('',(#8707));
#8709=SURFACE_STYLE_FILL_AREA(#8708);
#8710=SURFACE_SIDE_STYLE('',(#8709));
#8711=SURFACE_STYLE_USAGE(.BOTH.,#8710);
#8712=PRESENTATION_STYLE_ASSIGNMENT((#8711));
ENDSEC;
END-ISO-10303-21;
